ISO-10303-21;
HEADER;
/* Generated by software containing ST-Developer
 * from STEP Tools, Inc. (www.steptools.com) 
 */

FILE_DESCRIPTION(
/* description */ ('Spring compression tester'),
/* implementation_level */ '2;1');

FILE_NAME(
/* name */ 'M5x14 Cap Screw.step',
/* time_stamp */ '2026-10-28T03:24:11-07:00',
/* author */ (''),
/* organization */ (''),
/* preprocessor_version */ 'ST-DEVELOPER v20.2',
/* originating_system */ 'Autodesk Translation Framework v15.17.0.0',
/* authorisation */ '');

FILE_SCHEMA (('AUTOMOTIVE_DESIGN { 1 0 10303 214 3 1 1 }'));
ENDSEC;

DATA;
#10=MECHANICAL_DESIGN_GEOMETRIC_PRESENTATION_REPRESENTATION('',(#1126),#43521);
#931=ORIENTED_CLOSED_SHELL('',*,#18563,.F.);
#938=BREP_WITH_VOIDS('Body1',#18564,(#931));
#947=CONICAL_SURFACE('',#19981,0.4,0.785398163397448);
#948=CONICAL_SURFACE('',#19985,0.41,0.785398163397448);
#949=CONICAL_SURFACE('',#19989,0.26,0.463647609000806);
#1006=SHAPE_REPRESENTATION_RELATIONSHIP('SRR','None',#43818,#1066);
#1066=ADVANCED_BREP_SHAPE_REPRESENTATION('',(#938),#43478);
#1126=STYLED_ITEM('',(#44209),#938);
#1449=FACE_BOUND('',#3843,.T.);
#1877=PLANE('',#19969);
#1878=PLANE('',#19970);
#1879=PLANE('',#19971);
#1880=PLANE('',#19972);
#1881=PLANE('',#19973);
#1882=PLANE('',#19974);
#1883=PLANE('',#19975);
#1884=PLANE('',#19976);
#1885=PLANE('',#19977);
#1886=PLANE('',#19979);
#1887=PLANE('',#19987);
#2580=FACE_OUTER_BOUND('',#3829,.T.);
#2581=FACE_OUTER_BOUND('',#3830,.T.);
#2582=FACE_OUTER_BOUND('',#3831,.T.);
#2583=FACE_OUTER_BOUND('',#3832,.T.);
#2584=FACE_OUTER_BOUND('',#3833,.T.);
#2585=FACE_OUTER_BOUND('',#3834,.T.);
#2586=FACE_OUTER_BOUND('',#3835,.T.);
#2587=FACE_OUTER_BOUND('',#3836,.T.);
#2588=FACE_OUTER_BOUND('',#3837,.T.);
#2589=FACE_OUTER_BOUND('',#3838,.T.);
#2590=FACE_OUTER_BOUND('',#3839,.T.);
#2591=FACE_OUTER_BOUND('',#3840,.T.);
#2592=FACE_OUTER_BOUND('',#3841,.T.);
#2593=FACE_OUTER_BOUND('',#3842,.T.);
#2594=FACE_OUTER_BOUND('',#3844,.T.);
#2595=FACE_OUTER_BOUND('',#3845,.T.);
#3829=EDGE_LOOP('',(#14061,#14062,#14063,#14064));
#3830=EDGE_LOOP('',(#14065,#14066,#14067,#14068));
#3831=EDGE_LOOP('',(#14069,#14070,#14071,#14072));
#3832=EDGE_LOOP('',(#14073,#14074,#14075,#14076));
#3833=EDGE_LOOP('',(#14077,#14078,#14079,#14080));
#3834=EDGE_LOOP('',(#14081,#14082,#14083,#14084));
#3835=EDGE_LOOP('',(#14085,#14086,#14087,#14088,#14089,#14090));
#3836=EDGE_LOOP('',(#14091,#14092,#14093,#14094,#14095,#14096));
#3837=EDGE_LOOP('',(#14097));
#3838=EDGE_LOOP('',(#14098));
#3839=EDGE_LOOP('',(#14099,#14100,#14101,#14102));
#3840=EDGE_LOOP('',(#14103,#14104,#14105,#14106));
#3841=EDGE_LOOP('',(#14107,#14108,#14109,#14110));
#3842=EDGE_LOOP('',(#14111));
#3843=EDGE_LOOP('',(#14112));
#3844=EDGE_LOOP('',(#14113,#14114,#14115,#14116));
#3845=EDGE_LOOP('',(#14117,#14118,#14119,#14120));
#5278=LINE('',#28426,#6710);
#5279=LINE('',#28428,#6711);
#5280=LINE('',#28430,#6712);
#5281=LINE('',#28431,#6713);
#5282=LINE('',#28434,#6714);
#5283=LINE('',#28436,#6715);
#5284=LINE('',#28437,#6716);
#5285=LINE('',#28440,#6717);
#5286=LINE('',#28442,#6718);
#5287=LINE('',#28443,#6719);
#5288=LINE('',#28446,#6720);
#5289=LINE('',#28448,#6721);
#5290=LINE('',#28449,#6722);
#5291=LINE('',#28452,#6723);
#5292=LINE('',#28454,#6724);
#5293=LINE('',#28455,#6725);
#5294=LINE('',#28457,#6726);
#5295=LINE('',#28458,#6727);
#5296=LINE('',#28470,#6728);
#5297=LINE('',#28474,#6729);
#5298=LINE('',#28478,#6730);
#5299=LINE('',#28485,#6731);
#5300=LINE('',#28487,#6732);
#6710=VECTOR('',#23240,1.);
#6711=VECTOR('',#23241,1.);
#6712=VECTOR('',#23242,1.);
#6713=VECTOR('',#23243,1.);
#6714=VECTOR('',#23246,1.);
#6715=VECTOR('',#23247,1.);
#6716=VECTOR('',#23248,1.);
#6717=VECTOR('',#23251,1.);
#6718=VECTOR('',#23252,1.);
#6719=VECTOR('',#23253,1.);
#6720=VECTOR('',#23256,1.);
#6721=VECTOR('',#23257,1.);
#6722=VECTOR('',#23258,1.);
#6723=VECTOR('',#23261,1.);
#6724=VECTOR('',#23262,1.);
#6725=VECTOR('',#23263,1.);
#6726=VECTOR('',#23266,1.);
#6727=VECTOR('',#23267,1.);
#6728=VECTOR('',#23284,0.4);
#6729=VECTOR('',#23289,0.425);
#6730=VECTOR('',#23294,0.41);
#6731=VECTOR('',#23303,0.26);
#6732=VECTOR('',#23306,0.25);
#7720=CIRCLE('',#19978,0.24505);
#7721=CIRCLE('',#19980,0.375);
#7722=CIRCLE('',#19982,0.425);
#7723=CIRCLE('',#19984,0.425);
#7724=CIRCLE('',#19986,0.395);
#7725=CIRCLE('',#19988,0.27);
#7726=CIRCLE('',#19990,0.24505);
#8750=VERTEX_POINT('',#28424);
#8751=VERTEX_POINT('',#28425);
#8752=VERTEX_POINT('',#28427);
#8753=VERTEX_POINT('',#28429);
#8754=VERTEX_POINT('',#28433);
#8755=VERTEX_POINT('',#28435);
#8756=VERTEX_POINT('',#28439);
#8757=VERTEX_POINT('',#28441);
#8758=VERTEX_POINT('',#28445);
#8759=VERTEX_POINT('',#28447);
#8760=VERTEX_POINT('',#28451);
#8761=VERTEX_POINT('',#28453);
#8762=VERTEX_POINT('',#28462);
#8763=VERTEX_POINT('',#28465);
#8764=VERTEX_POINT('',#28468);
#8765=VERTEX_POINT('',#28472);
#8766=VERTEX_POINT('',#28476);
#8767=VERTEX_POINT('',#28480);
#8768=VERTEX_POINT('',#28483);
#10695=EDGE_CURVE('',#8750,#8751,#5278,.T.);
#10696=EDGE_CURVE('',#8751,#8752,#5279,.T.);
#10697=EDGE_CURVE('',#8752,#8753,#5280,.T.);
#10698=EDGE_CURVE('',#8750,#8753,#5281,.T.);
#10699=EDGE_CURVE('',#8751,#8754,#5282,.T.);
#10700=EDGE_CURVE('',#8754,#8755,#5283,.T.);
#10701=EDGE_CURVE('',#8755,#8752,#5284,.T.);
#10702=EDGE_CURVE('',#8754,#8756,#5285,.T.);
#10703=EDGE_CURVE('',#8756,#8757,#5286,.T.);
#10704=EDGE_CURVE('',#8757,#8755,#5287,.T.);
#10705=EDGE_CURVE('',#8756,#8758,#5288,.T.);
#10706=EDGE_CURVE('',#8758,#8759,#5289,.T.);
#10707=EDGE_CURVE('',#8759,#8757,#5290,.T.);
#10708=EDGE_CURVE('',#8758,#8760,#5291,.T.);
#10709=EDGE_CURVE('',#8760,#8761,#5292,.T.);
#10710=EDGE_CURVE('',#8761,#8759,#5293,.T.);
#10711=EDGE_CURVE('',#8760,#8750,#5294,.T.);
#10712=EDGE_CURVE('',#8753,#8761,#5295,.T.);
#10713=EDGE_CURVE('',#8762,#8762,#7720,.T.);
#10714=EDGE_CURVE('',#8763,#8763,#7721,.T.);
#10715=EDGE_CURVE('',#8764,#8764,#7722,.T.);
#10716=EDGE_CURVE('',#8764,#8763,#5296,.T.);
#10717=EDGE_CURVE('',#8765,#8765,#7723,.T.);
#10718=EDGE_CURVE('',#8765,#8764,#5297,.T.);
#10719=EDGE_CURVE('',#8766,#8766,#7724,.T.);
#10720=EDGE_CURVE('',#8766,#8765,#5298,.T.);
#10721=EDGE_CURVE('',#8767,#8767,#7725,.T.);
#10722=EDGE_CURVE('',#8768,#8768,#7726,.F.);
#10723=EDGE_CURVE('',#8768,#8767,#5299,.T.);
#10724=EDGE_CURVE('',#8762,#8768,#5300,.T.);
#14061=ORIENTED_EDGE('',*,*,#10695,.T.);
#14062=ORIENTED_EDGE('',*,*,#10696,.T.);
#14063=ORIENTED_EDGE('',*,*,#10697,.T.);
#14064=ORIENTED_EDGE('',*,*,#10698,.F.);
#14065=ORIENTED_EDGE('',*,*,#10699,.T.);
#14066=ORIENTED_EDGE('',*,*,#10700,.T.);
#14067=ORIENTED_EDGE('',*,*,#10701,.T.);
#14068=ORIENTED_EDGE('',*,*,#10696,.F.);
#14069=ORIENTED_EDGE('',*,*,#10702,.T.);
#14070=ORIENTED_EDGE('',*,*,#10703,.T.);
#14071=ORIENTED_EDGE('',*,*,#10704,.T.);
#14072=ORIENTED_EDGE('',*,*,#10700,.F.);
#14073=ORIENTED_EDGE('',*,*,#10705,.T.);
#14074=ORIENTED_EDGE('',*,*,#10706,.T.);
#14075=ORIENTED_EDGE('',*,*,#10707,.T.);
#14076=ORIENTED_EDGE('',*,*,#10703,.F.);
#14077=ORIENTED_EDGE('',*,*,#10708,.T.);
#14078=ORIENTED_EDGE('',*,*,#10709,.T.);
#14079=ORIENTED_EDGE('',*,*,#10710,.T.);
#14080=ORIENTED_EDGE('',*,*,#10706,.F.);
#14081=ORIENTED_EDGE('',*,*,#10711,.T.);
#14082=ORIENTED_EDGE('',*,*,#10698,.T.);
#14083=ORIENTED_EDGE('',*,*,#10712,.T.);
#14084=ORIENTED_EDGE('',*,*,#10709,.F.);
#14085=ORIENTED_EDGE('',*,*,#10711,.F.);
#14086=ORIENTED_EDGE('',*,*,#10708,.F.);
#14087=ORIENTED_EDGE('',*,*,#10705,.F.);
#14088=ORIENTED_EDGE('',*,*,#10702,.F.);
#14089=ORIENTED_EDGE('',*,*,#10699,.F.);
#14090=ORIENTED_EDGE('',*,*,#10695,.F.);
#14091=ORIENTED_EDGE('',*,*,#10712,.F.);
#14092=ORIENTED_EDGE('',*,*,#10697,.F.);
#14093=ORIENTED_EDGE('',*,*,#10701,.F.);
#14094=ORIENTED_EDGE('',*,*,#10704,.F.);
#14095=ORIENTED_EDGE('',*,*,#10707,.F.);
#14096=ORIENTED_EDGE('',*,*,#10710,.F.);
#14097=ORIENTED_EDGE('',*,*,#10713,.F.);
#14098=ORIENTED_EDGE('',*,*,#10714,.F.);
#14099=ORIENTED_EDGE('',*,*,#10715,.F.);
#14100=ORIENTED_EDGE('',*,*,#10716,.T.);
#14101=ORIENTED_EDGE('',*,*,#10714,.T.);
#14102=ORIENTED_EDGE('',*,*,#10716,.F.);
#14103=ORIENTED_EDGE('',*,*,#10717,.F.);
#14104=ORIENTED_EDGE('',*,*,#10718,.T.);
#14105=ORIENTED_EDGE('',*,*,#10715,.T.);
#14106=ORIENTED_EDGE('',*,*,#10718,.F.);
#14107=ORIENTED_EDGE('',*,*,#10719,.F.);
#14108=ORIENTED_EDGE('',*,*,#10720,.T.);
#14109=ORIENTED_EDGE('',*,*,#10717,.T.);
#14110=ORIENTED_EDGE('',*,*,#10720,.F.);
#14111=ORIENTED_EDGE('',*,*,#10719,.T.);
#14112=ORIENTED_EDGE('',*,*,#10721,.F.);
#14113=ORIENTED_EDGE('',*,*,#10722,.F.);
#14114=ORIENTED_EDGE('',*,*,#10723,.T.);
#14115=ORIENTED_EDGE('',*,*,#10721,.T.);
#14116=ORIENTED_EDGE('',*,*,#10723,.F.);
#14117=ORIENTED_EDGE('',*,*,#10713,.T.);
#14118=ORIENTED_EDGE('',*,*,#10724,.T.);
#14119=ORIENTED_EDGE('',*,*,#10722,.T.);
#14120=ORIENTED_EDGE('',*,*,#10724,.F.);
#17225=CYLINDRICAL_SURFACE('',#19983,0.425);
#17226=CYLINDRICAL_SURFACE('',#19991,0.24505);
#17904=ADVANCED_FACE('',(#2580),#1877,.F.);
#17905=ADVANCED_FACE('',(#2581),#1878,.F.);
#17906=ADVANCED_FACE('',(#2582),#1879,.F.);
#17907=ADVANCED_FACE('',(#2583),#1880,.F.);
#17908=ADVANCED_FACE('',(#2584),#1881,.F.);
#17909=ADVANCED_FACE('',(#2585),#1882,.F.);
#17910=ADVANCED_FACE('',(#2586),#1883,.F.);
#17911=ADVANCED_FACE('',(#2587),#1884,.F.);
#17912=ADVANCED_FACE('',(#2588),#1885,.F.);
#17913=ADVANCED_FACE('',(#2589),#1886,.T.);
#17914=ADVANCED_FACE('',(#2590),#947,.T.);
#17915=ADVANCED_FACE('',(#2591),#17225,.T.);
#17916=ADVANCED_FACE('',(#2592),#948,.T.);
#17917=ADVANCED_FACE('',(#2593,#1449),#1887,.T.);
#17918=ADVANCED_FACE('',(#2594),#949,.T.);
#17919=ADVANCED_FACE('',(#2595),#17226,.T.);
#18563=CLOSED_SHELL('',(#17904,#17905,#17906,#17907,#17908,#17909,#17910,
#17911));
#18564=CLOSED_SHELL('',(#17912,#17913,#17914,#17915,#17916,#17917,#17918,
#17919));
#19968=AXIS2_PLACEMENT_3D('',#28422,#23236,#23237);
#19969=AXIS2_PLACEMENT_3D('',#28423,#23238,#23239);
#19970=AXIS2_PLACEMENT_3D('',#28432,#23244,#23245);
#19971=AXIS2_PLACEMENT_3D('',#28438,#23249,#23250);
#19972=AXIS2_PLACEMENT_3D('',#28444,#23254,#23255);
#19973=AXIS2_PLACEMENT_3D('',#28450,#23259,#23260);
#19974=AXIS2_PLACEMENT_3D('',#28456,#23264,#23265);
#19975=AXIS2_PLACEMENT_3D('',#28459,#23268,#23269);
#19976=AXIS2_PLACEMENT_3D('',#28460,#23270,#23271);
#19977=AXIS2_PLACEMENT_3D('',#28461,#23272,#23273);
#19978=AXIS2_PLACEMENT_3D('',#28463,#23274,#23275);
#19979=AXIS2_PLACEMENT_3D('',#28464,#23276,#23277);
#19980=AXIS2_PLACEMENT_3D('',#28466,#23278,#23279);
#19981=AXIS2_PLACEMENT_3D('',#28467,#23280,#23281);
#19982=AXIS2_PLACEMENT_3D('',#28469,#23282,#23283);
#19983=AXIS2_PLACEMENT_3D('',#28471,#23285,#23286);
#19984=AXIS2_PLACEMENT_3D('',#28473,#23287,#23288);
#19985=AXIS2_PLACEMENT_3D('',#28475,#23290,#23291);
#19986=AXIS2_PLACEMENT_3D('',#28477,#23292,#23293);
#19987=AXIS2_PLACEMENT_3D('',#28479,#23295,#23296);
#19988=AXIS2_PLACEMENT_3D('',#28481,#23297,#23298);
#19989=AXIS2_PLACEMENT_3D('',#28482,#23299,#23300);
#19990=AXIS2_PLACEMENT_3D('',#28484,#23301,#23302);
#19991=AXIS2_PLACEMENT_3D('',#28486,#23304,#23305);
#23236=DIRECTION('axis',(0.,0.,1.));
#23237=DIRECTION('refdir',(1.,0.,0.));
#23238=DIRECTION('center_axis',(0.866025403784439,0.,-0.5));
#23239=DIRECTION('ref_axis',(0.5,0.,0.866025403784439));
#23240=DIRECTION('',(-0.5,0.,-0.866025403784439));
#23241=DIRECTION('',(0.,-1.,0.));
#23242=DIRECTION('',(0.5,0.,0.866025403784439));
#23243=DIRECTION('',(0.,-1.,0.));
#23244=DIRECTION('center_axis',(1.20185167898973E-16,0.,-1.));
#23245=DIRECTION('ref_axis',(1.,0.,1.20185167898973E-16));
#23246=DIRECTION('',(-1.,0.,-1.20185167898973E-16));
#23247=DIRECTION('',(0.,-1.,0.));
#23248=DIRECTION('',(1.,0.,1.20185167898973E-16));
#23249=DIRECTION('center_axis',(-0.866025403784439,0.,-0.5));
#23250=DIRECTION('ref_axis',(0.5,0.,-0.866025403784439));
#23251=DIRECTION('',(-0.5,0.,0.866025403784439));
#23252=DIRECTION('',(0.,-1.,0.));
#23253=DIRECTION('',(0.5,0.,-0.866025403784439));
#23254=DIRECTION('center_axis',(-0.866025403784439,0.,0.5));
#23255=DIRECTION('ref_axis',(-0.5,0.,-0.866025403784439));
#23256=DIRECTION('',(0.5,0.,0.866025403784439));
#23257=DIRECTION('',(0.,-1.,0.));
#23258=DIRECTION('',(-0.5,0.,-0.866025403784439));
#23259=DIRECTION('center_axis',(-2.40370335797945E-16,0.,1.));
#23260=DIRECTION('ref_axis',(-1.,0.,-2.40370335797945E-16));
#23261=DIRECTION('',(1.,0.,2.40370335797945E-16));
#23262=DIRECTION('',(0.,-1.,0.));
#23263=DIRECTION('',(-1.,0.,-2.40370335797945E-16));
#23264=DIRECTION('center_axis',(0.866025403784439,0.,0.5));
#23265=DIRECTION('ref_axis',(-0.5,0.,0.866025403784439));
#23266=DIRECTION('',(0.5,0.,-0.866025403784439));
#23267=DIRECTION('',(-0.5,0.,0.866025403784439));
#23268=DIRECTION('center_axis',(0.,1.,0.));
#23269=DIRECTION('ref_axis',(1.,0.,0.));
#23270=DIRECTION('center_axis',(0.,-1.,0.));
#23271=DIRECTION('ref_axis',(0.,0.,-1.));
#23272=DIRECTION('center_axis',(0.,1.,0.));
#23273=DIRECTION('ref_axis',(1.,0.,0.));
#23274=DIRECTION('center_axis',(0.,1.,0.));
#23275=DIRECTION('ref_axis',(1.,0.,0.));
#23276=DIRECTION('center_axis',(0.,1.,0.));
#23277=DIRECTION('ref_axis',(0.,0.,1.));
#23278=DIRECTION('center_axis',(0.,-1.,0.));
#23279=DIRECTION('ref_axis',(1.,0.,0.));
#23280=DIRECTION('center_axis',(0.,-1.,0.));
#23281=DIRECTION('ref_axis',(1.,0.,0.));
#23282=DIRECTION('center_axis',(0.,-1.,0.));
#23283=DIRECTION('ref_axis',(1.,0.,0.));
#23284=DIRECTION('',(0.707106781186548,0.707106781186547,8.65956056235493E-17));
#23285=DIRECTION('center_axis',(0.,-1.,0.));
#23286=DIRECTION('ref_axis',(1.,0.,0.));
#23287=DIRECTION('center_axis',(0.,-1.,0.));
#23288=DIRECTION('ref_axis',(1.,0.,0.));
#23289=DIRECTION('',(0.,1.,0.));
#23290=DIRECTION('center_axis',(0.,1.,0.));
#23291=DIRECTION('ref_axis',(1.,0.,0.));
#23292=DIRECTION('center_axis',(0.,-1.,0.));
#23293=DIRECTION('ref_axis',(1.,0.,0.));
#23294=DIRECTION('',(-0.707106781186547,0.707106781186548,-8.65956056235493E-17));
#23295=DIRECTION('center_axis',(0.,-1.,0.));
#23296=DIRECTION('ref_axis',(0.,0.,-1.));
#23297=DIRECTION('center_axis',(0.,-1.,0.));
#23298=DIRECTION('ref_axis',(1.,0.,0.));
#23299=DIRECTION('center_axis',(0.,1.,0.));
#23300=DIRECTION('ref_axis',(1.,0.,0.));
#23301=DIRECTION('center_axis',(0.,1.,0.));
#23302=DIRECTION('ref_axis',(1.,0.,0.));
#23303=DIRECTION('',(-0.447213595499958,0.894427190999916,-5.47678698264203E-17));
#23304=DIRECTION('center_axis',(0.,-1.,0.));
#23305=DIRECTION('ref_axis',(1.,0.,0.));
#23306=DIRECTION('',(0.,1.,0.));
#28422=CARTESIAN_POINT('',(0.,0.,0.));
#28423=CARTESIAN_POINT('Origin',(0.115470053837925,-0.5,-0.2));
#28424=CARTESIAN_POINT('',(0.23094010767585,-0.5,0.));
#28425=CARTESIAN_POINT('',(0.115470053837925,-0.5,-0.2));
#28426=CARTESIAN_POINT('',(0.23094010767585,-0.5,0.));
#28427=CARTESIAN_POINT('',(0.115470053837925,-0.8,-0.2));
#28428=CARTESIAN_POINT('',(0.115470053837925,-0.5,-0.2));
#28429=CARTESIAN_POINT('',(0.23094010767585,-0.8,0.));
#28430=CARTESIAN_POINT('',(0.23094010767585,-0.8,0.));
#28431=CARTESIAN_POINT('',(0.23094010767585,-0.5,0.));
#28432=CARTESIAN_POINT('Origin',(-0.115470053837925,-0.5,-0.2));
#28433=CARTESIAN_POINT('',(-0.115470053837925,-0.5,-0.2));
#28434=CARTESIAN_POINT('',(0.115470053837925,-0.5,-0.2));
#28435=CARTESIAN_POINT('',(-0.115470053837925,-0.8,-0.2));
#28436=CARTESIAN_POINT('',(-0.115470053837925,-0.5,-0.2));
#28437=CARTESIAN_POINT('',(0.115470053837925,-0.8,-0.2));
#28438=CARTESIAN_POINT('Origin',(-0.23094010767585,-0.5,-2.77555756156289E-17));
#28439=CARTESIAN_POINT('',(-0.23094010767585,-0.5,-2.82820063659975E-17));
#28440=CARTESIAN_POINT('',(-0.115470053837925,-0.5,-0.2));
#28441=CARTESIAN_POINT('',(-0.23094010767585,-0.8,-2.77555756156289E-17));
#28442=CARTESIAN_POINT('',(-0.23094010767585,-0.5,-2.82820063659975E-17));
#28443=CARTESIAN_POINT('',(-0.115470053837925,-0.8,-0.2));
#28444=CARTESIAN_POINT('Origin',(-0.115470053837925,-0.5,0.2));
#28445=CARTESIAN_POINT('',(-0.115470053837925,-0.5,0.2));
#28446=CARTESIAN_POINT('',(-0.23094010767585,-0.5,-2.82820063659975E-17));
#28447=CARTESIAN_POINT('',(-0.115470053837925,-0.8,0.2));
#28448=CARTESIAN_POINT('',(-0.115470053837925,-0.5,0.2));
#28449=CARTESIAN_POINT('',(-0.23094010767585,-0.8,-2.82820063659975E-17));
#28450=CARTESIAN_POINT('Origin',(0.115470053837925,-0.5,0.2));
#28451=CARTESIAN_POINT('',(0.115470053837925,-0.5,0.2));
#28452=CARTESIAN_POINT('',(-0.115470053837925,-0.5,0.2));
#28453=CARTESIAN_POINT('',(0.115470053837925,-0.8,0.2));
#28454=CARTESIAN_POINT('',(0.115470053837925,-0.5,0.2));
#28455=CARTESIAN_POINT('',(-0.115470053837925,-0.8,0.2));
#28456=CARTESIAN_POINT('Origin',(0.23094010767585,-0.5,0.));
#28457=CARTESIAN_POINT('',(0.115470053837925,-0.5,0.2));
#28458=CARTESIAN_POINT('',(0.115470053837925,-0.8,0.2));
#28459=CARTESIAN_POINT('Origin',(0.,-0.5,0.));
#28460=CARTESIAN_POINT('Origin',(0.,-0.8,0.));
#28461=CARTESIAN_POINT('Origin',(0.,-1.4,0.));
#28462=CARTESIAN_POINT('',(-0.24505,-1.4,3.00099698131059E-17));
#28463=CARTESIAN_POINT('Origin',(0.,-1.4,0.));
#28464=CARTESIAN_POINT('Origin',(0.375,0.5,0.));
#28465=CARTESIAN_POINT('',(-0.375,0.5,-4.59242549680257E-17));
#28466=CARTESIAN_POINT('Origin',(0.,0.5,0.));
#28467=CARTESIAN_POINT('Origin',(0.,0.475,0.));
#28468=CARTESIAN_POINT('',(-0.425,0.45,-5.20474889637625E-17));
#28469=CARTESIAN_POINT('Origin',(0.,0.45,0.));
#28470=CARTESIAN_POINT('',(-0.4,0.475,-4.89858719658941E-17));
#28471=CARTESIAN_POINT('Origin',(0.,0.24,0.));
#28472=CARTESIAN_POINT('',(-0.425,0.0299999999999998,-5.20474889637625E-17));
#28473=CARTESIAN_POINT('Origin',(0.,0.0299999999999998,0.));
#28474=CARTESIAN_POINT('',(-0.425,0.24,-5.20474889637625E-17));
#28475=CARTESIAN_POINT('Origin',(0.,0.0150000000000001,0.));
#28476=CARTESIAN_POINT('',(-0.395,4.85722573273506E-17,-4.83735485663204E-17));
#28477=CARTESIAN_POINT('Origin',(0.,0.,0.));
#28478=CARTESIAN_POINT('',(-0.41,0.0150000000000001,-5.02105187650415E-17));
#28479=CARTESIAN_POINT('Origin',(0.27,0.,0.));
#28480=CARTESIAN_POINT('',(-0.27,0.,-3.30654635769785E-17));
#28481=CARTESIAN_POINT('Origin',(0.,0.,0.));
#28482=CARTESIAN_POINT('Origin',(0.,-0.02,0.));
#28483=CARTESIAN_POINT('',(-0.24505,-0.0498999999999999,3.00099698131059E-17));
#28484=CARTESIAN_POINT('Origin',(0.,-0.0498999999999999,0.));
#28485=CARTESIAN_POINT('',(-0.26,-0.02,-3.18408167778312E-17));
#28486=CARTESIAN_POINT('Origin',(0.,-0.995,0.));
#28487=CARTESIAN_POINT('',(-0.24505,-0.995,-3.00099698131059E-17));
#43410=UNCERTAINTY_MEASURE_WITH_UNIT(LENGTH_MEASURE(0.001),#43522,
'DISTANCE_ACCURACY_VALUE',
'Maximum model space distance between geometric entities at asserted c
onnectivities');
#43453=UNCERTAINTY_MEASURE_WITH_UNIT(LENGTH_MEASURE(0.001),#43522,
'DISTANCE_ACCURACY_VALUE',
'Maximum model space distance between geometric entities at asserted c
onnectivities');
#43478=(
GEOMETRIC_REPRESENTATION_CONTEXT(3)
GLOBAL_UNCERTAINTY_ASSIGNED_CONTEXT((#43410))
GLOBAL_UNIT_ASSIGNED_CONTEXT((#43522,#43524,#43525))
REPRESENTATION_CONTEXT('','3D')
);
#43521=(
GEOMETRIC_REPRESENTATION_CONTEXT(3)
GLOBAL_UNCERTAINTY_ASSIGNED_CONTEXT((#43453))
GLOBAL_UNIT_ASSIGNED_CONTEXT((#43522,#43524,#43525))
REPRESENTATION_CONTEXT('','3D')
);
#43522=(
LENGTH_UNIT()
NAMED_UNIT(*)
SI_UNIT(.CENTI.,.METRE.)
);
#43524=(
NAMED_UNIT(*)
PLANE_ANGLE_UNIT()
SI_UNIT($,.RADIAN.)
);
#43525=(
NAMED_UNIT(*)
SI_UNIT($,.STERADIAN.)
SOLID_ANGLE_UNIT()
);
#43550=SHAPE_DEFINITION_REPRESENTATION(#43617,#43818);
#43617=PRODUCT_DEFINITION_SHAPE('',$,#43886);
#43818=SHAPE_REPRESENTATION('',(#19968),#43478);
#43861=PRODUCT_DEFINITION_CONTEXT('part definition',#44064,'design');
#43886=PRODUCT_DEFINITION('M5x14 Cap Screw','M5x14 Cap Screw',#43953,#43861);
#43953=PRODUCT_DEFINITION_FORMATION('',$,#44090);
#44064=APPLICATION_CONTEXT(
'Core Data for Automotive Mechanical Design Process');
#44065=PRODUCT_CONTEXT('part definition',#44064,'mechanical');
#44090=PRODUCT('M5x14 Cap Screw','M5x14 Cap Screw','M5x14 Cap Screw',(#44065));
#44203=COLOUR_RGB('Black',0.12,0.14,0.17);
#44204=FILL_AREA_STYLE_COLOUR('',#44203);
#44205=FILL_AREA_STYLE('',(#44204));
#44206=SURFACE_STYLE_FILL_AREA(#44205);
#44207=SURFACE_SIDE_STYLE('',(#44206));
#44208=SURFACE_STYLE_USAGE(.BOTH.,#44207);
#44209=PRESENTATION_STYLE_ASSIGNMENT((#44208));
ENDSEC;
END-ISO-10303-21;
